ISO-10303-21;
HEADER;
/* Generated by software containing ST-Developer
 * from STEP Tools, Inc. (www.steptools.com) 
 */

FILE_DESCRIPTION(
/* description */ ('Independent compact industrial fixture table, bolted aluminum worktop
 on connected adjustable support base. Whole-mm nominal dimensions. No
 load rating assigned.'),
/* implementation_level */ '2;1');

FILE_NAME(
/* name */ 'Flat washer M6.step',
/* time_stamp */ '2026-11-07T17:47:58-08:00',
/* author */ (''),
/* organization */ (''),
/* preprocessor_version */ 'ST-DEVELOPER v20.2',
/* originating_system */ 'Autodesk Translation Framework v15.17.0.0',
/* authorisation */ '');

FILE_SCHEMA (('AUTOMOTIVE_DESIGN { 1 0 10303 214 3 1 1 }'));
ENDSEC;

DATA;
#10=MECHANICAL_DESIGN_GEOMETRIC_PRESENTATION_REPRESENTATION('',(#2268),#97475);
#2230=SHAPE_REPRESENTATION_RELATIONSHIP('SRR','None',#97624,#2249);
#2249=ADVANCED_BREP_SHAPE_REPRESENTATION('',(#2287),#97474);
#2268=STYLED_ITEM('',(#97721),#2287);
#2287=MANIFOLD_SOLID_BREP('Body1',#21829);
#2377=FACE_BOUND('',#4933,.T.);
#2378=FACE_BOUND('',#4935,.T.);
#2535=PLANE('',#23461);
#2536=PLANE('',#23462);
#3687=FACE_OUTER_BOUND('',#4930,.T.);
#3688=FACE_OUTER_BOUND('',#4931,.T.);
#3689=FACE_OUTER_BOUND('',#4932,.T.);
#3690=FACE_OUTER_BOUND('',#4934,.T.);
#4930=EDGE_LOOP('',(#19698,#19699,#19700,#19701));
#4931=EDGE_LOOP('',(#19702,#19703,#19704,#19705));
#4932=EDGE_LOOP('',(#19706));
#4933=EDGE_LOOP('',(#19707));
#4934=EDGE_LOOP('',(#19708));
#4935=EDGE_LOOP('',(#19709));
#6148=LINE('',#97381,#7362);
#6149=LINE('',#97387,#7363);
#7362=VECTOR('',#27548,3.5);
#7363=VECTOR('',#27555,7.);
#7609=CIRCLE('',#23456,3.5);
#7610=CIRCLE('',#23457,3.5);
#7611=CIRCLE('',#23459,7.);
#7612=CIRCLE('',#23460,7.);
#9809=VERTEX_POINT('',#97378);
#9810=VERTEX_POINT('',#97380);
#9811=VERTEX_POINT('',#97384);
#9812=VERTEX_POINT('',#97386);
#13106=EDGE_CURVE('',#9809,#9809,#7609,.T.);
#13107=EDGE_CURVE('',#9809,#9810,#6148,.T.);
#13108=EDGE_CURVE('',#9810,#9810,#7610,.T.);
#13109=EDGE_CURVE('',#9811,#9811,#7611,.T.);
#13110=EDGE_CURVE('',#9811,#9812,#6149,.T.);
#13111=EDGE_CURVE('',#9812,#9812,#7612,.T.);
#19698=ORIENTED_EDGE('',*,*,#13106,.F.);
#19699=ORIENTED_EDGE('',*,*,#13107,.T.);
#19700=ORIENTED_EDGE('',*,*,#13108,.T.);
#19701=ORIENTED_EDGE('',*,*,#13107,.F.);
#19702=ORIENTED_EDGE('',*,*,#13109,.F.);
#19703=ORIENTED_EDGE('',*,*,#13110,.T.);
#19704=ORIENTED_EDGE('',*,*,#13111,.T.);
#19705=ORIENTED_EDGE('',*,*,#13110,.F.);
#19706=ORIENTED_EDGE('',*,*,#13109,.T.);
#19707=ORIENTED_EDGE('',*,*,#13106,.T.);
#19708=ORIENTED_EDGE('',*,*,#13111,.F.);
#19709=ORIENTED_EDGE('',*,*,#13108,.F.);
#20655=CYLINDRICAL_SURFACE('',#23455,3.5);
#20656=CYLINDRICAL_SURFACE('',#23458,7.);
#21807=ADVANCED_FACE('',(#3687),#20655,.F.);
#21808=ADVANCED_FACE('',(#3688),#20656,.T.);
#21809=ADVANCED_FACE('',(#3689,#2377),#2535,.T.);
#21810=ADVANCED_FACE('',(#3690,#2378),#2536,.F.);
#21829=CLOSED_SHELL('',(#21807,#21808,#21809,#21810));
#23454=AXIS2_PLACEMENT_3D('',#97376,#27542,#27543);
#23455=AXIS2_PLACEMENT_3D('',#97377,#27544,#27545);
#23456=AXIS2_PLACEMENT_3D('',#97379,#27546,#27547);
#23457=AXIS2_PLACEMENT_3D('',#97382,#27549,#27550);
#23458=AXIS2_PLACEMENT_3D('',#97383,#27551,#27552);
#23459=AXIS2_PLACEMENT_3D('',#97385,#27553,#27554);
#23460=AXIS2_PLACEMENT_3D('',#97388,#27556,#27557);
#23461=AXIS2_PLACEMENT_3D('',#97389,#27558,#27559);
#23462=AXIS2_PLACEMENT_3D('',#97390,#27560,#27561);
#27542=DIRECTION('axis',(0.,0.,1.));
#27543=DIRECTION('refdir',(1.,0.,0.));
#27544=DIRECTION('center_axis',(0.,0.,1.));
#27545=DIRECTION('ref_axis',(1.,0.,0.));
#27546=DIRECTION('center_axis',(0.,0.,-1.));
#27547=DIRECTION('ref_axis',(1.,0.,0.));
#27548=DIRECTION('',(0.,0.,-1.));
#27549=DIRECTION('center_axis',(0.,0.,-1.));
#27550=DIRECTION('ref_axis',(1.,0.,0.));
#27551=DIRECTION('center_axis',(0.,0.,1.));
#27552=DIRECTION('ref_axis',(1.,0.,0.));
#27553=DIRECTION('center_axis',(0.,0.,1.));
#27554=DIRECTION('ref_axis',(1.,0.,0.));
#27555=DIRECTION('',(0.,0.,-1.));
#27556=DIRECTION('center_axis',(0.,0.,1.));
#27557=DIRECTION('ref_axis',(1.,0.,0.));
#27558=DIRECTION('center_axis',(0.,0.,1.));
#27559=DIRECTION('ref_axis',(1.,0.,0.));
#27560=DIRECTION('center_axis',(0.,0.,1.));
#27561=DIRECTION('ref_axis',(1.,0.,0.));
#97376=CARTESIAN_POINT('',(0.,0.,0.));
#97377=CARTESIAN_POINT('Origin',(0.,0.,0.));
#97378=CARTESIAN_POINT('',(-3.5,-4.28626379701574E-16,2.));
#97379=CARTESIAN_POINT('Origin',(0.,0.,2.));
#97380=CARTESIAN_POINT('',(-3.5,-4.28626379701574E-16,0.));
#97381=CARTESIAN_POINT('',(-3.5,-4.28626379701574E-16,0.));
#97382=CARTESIAN_POINT('Origin',(0.,0.,0.));
#97383=CARTESIAN_POINT('Origin',(0.,0.,0.));
#97384=CARTESIAN_POINT('',(-7.,-8.57252759403147E-16,2.));
#97385=CARTESIAN_POINT('Origin',(0.,0.,2.));
#97386=CARTESIAN_POINT('',(-7.,-8.57252759403147E-16,0.));
#97387=CARTESIAN_POINT('',(-7.,-8.57252759403147E-16,0.));
#97388=CARTESIAN_POINT('Origin',(0.,0.,0.));
#97389=CARTESIAN_POINT('Origin',(0.,0.,2.));
#97390=CARTESIAN_POINT('Origin',(0.,0.,0.));
#97451=UNCERTAINTY_MEASURE_WITH_UNIT(LENGTH_MEASURE(0.01),#97476,
'DISTANCE_ACCURACY_VALUE',
'Maximum model space distance between geometric entities at asserted c
onnectivities');
#97452=UNCERTAINTY_MEASURE_WITH_UNIT(LENGTH_MEASURE(0.01),#97476,
'DISTANCE_ACCURACY_VALUE',
'Maximum model space distance between geometric entities at asserted c
onnectivities');
#97474=(
GEOMETRIC_REPRESENTATION_CONTEXT(3)
GLOBAL_UNCERTAINTY_ASSIGNED_CONTEXT((#97451))
GLOBAL_UNIT_ASSIGNED_CONTEXT((#97476,#97478,#97479))
REPRESENTATION_CONTEXT('','3D')
);
#97475=(
GEOMETRIC_REPRESENTATION_CONTEXT(3)
GLOBAL_UNCERTAINTY_ASSIGNED_CONTEXT((#97452))
GLOBAL_UNIT_ASSIGNED_CONTEXT((#97476,#97478,#97479))
REPRESENTATION_CONTEXT('','3D')
);
#97476=(
LENGTH_UNIT()
NAMED_UNIT(*)
SI_UNIT(.MILLI.,.METRE.)
);
#97478=(
NAMED_UNIT(*)
PLANE_ANGLE_UNIT()
SI_UNIT($,.RADIAN.)
);
#97479=(
NAMED_UNIT(*)
SI_UNIT($,.STERADIAN.)
SOLID_ANGLE_UNIT()
);
#97501=SHAPE_DEFINITION_REPRESENTATION(#97563,#97624);
#97563=PRODUCT_DEFINITION_SHAPE('',$,#97647);
#97624=SHAPE_REPRESENTATION('',(#23454),#97474);
#97625=PRODUCT_DEFINITION_CONTEXT('part definition',#97693,'design');
#97647=PRODUCT_DEFINITION('Flat washer M6','Flat washer M6',#97669,#97625);
#97669=PRODUCT_DEFINITION_FORMATION('',$,#97716);
#97693=APPLICATION_CONTEXT(
'Core Data for Automotive Mechanical Design Process');
#97694=PRODUCT_CONTEXT('part definition',#97693,'mechanical');
#97716=PRODUCT('Flat washer M6','Flat washer M6',$,(#97694));
#97721=PRESENTATION_STYLE_ASSIGNMENT((#97728));
#97728=SURFACE_STYLE_USAGE(.BOTH.,#97735);
#97735=SURFACE_SIDE_STYLE('',(#97742));
#97742=SURFACE_STYLE_FILL_AREA(#97749);
#97749=FILL_AREA_STYLE('Light gray',(#97756));
#97756=FILL_AREA_STYLE_COLOUR('Light gray',#97763);
#97763=COLOUR_RGB('Light gray',0.725490196078431,0.752941176470588,0.792156862745098);
ENDSEC;
END-ISO-10303-21;
